ISO-10303-21;
HEADER;
/* Generated by software containing ST-Developer
 * from STEP Tools, Inc. (www.steptools.com) 
 */

FILE_DESCRIPTION(
/* description */ ('Turntable on roller ring'),
/* implementation_level */ '2;1');

FILE_NAME(
/* name */ 'Inner race spacer (2).step',
/* time_stamp */ '2026-10-28T03:23:59-07:00',
/* author */ (''),
/* organization */ (''),
/* preprocessor_version */ 'ST-DEVELOPER v20.2',
/* originating_system */ 'Autodesk Translation Framework v15.17.0.0',
/* authorisation */ '');

FILE_SCHEMA (('AUTOMOTIVE_DESIGN { 1 0 10303 214 3 1 1 }'));
ENDSEC;

DATA;
#10=MECHANICAL_DESIGN_GEOMETRIC_PRESENTATION_REPRESENTATION('',(#649),#16281);
#530=SHAPE_REPRESENTATION_RELATIONSHIP('SRR','None',#16548,#585);
#585=ADVANCED_BREP_SHAPE_REPRESENTATION('',(#719),#16242);
#649=STYLED_ITEM('',(#16932),#719);
#719=MANIFOLD_SOLID_BREP('Body1',#8392);
#905=FACE_BOUND('',#2186,.T.);
#906=FACE_BOUND('',#2188,.T.);
#1129=PLANE('',#9666);
#1130=PLANE('',#9667);
#1530=FACE_OUTER_BOUND('',#2183,.T.);
#1531=FACE_OUTER_BOUND('',#2184,.T.);
#1532=FACE_OUTER_BOUND('',#2185,.T.);
#1533=FACE_OUTER_BOUND('',#2187,.T.);
#2183=EDGE_LOOP('',(#6833,#6834,#6835,#6836));
#2184=EDGE_LOOP('',(#6837,#6838,#6839,#6840));
#2185=EDGE_LOOP('',(#6841));
#2186=EDGE_LOOP('',(#6842));
#2187=EDGE_LOOP('',(#6843));
#2188=EDGE_LOOP('',(#6844));
#2782=LINE('',#14772,#3265);
#2783=LINE('',#14778,#3266);
#3265=VECTOR('',#11733,0.505);
#3266=VECTOR('',#11740,0.7);
#3743=CIRCLE('',#9661,0.505);
#3744=CIRCLE('',#9662,0.505);
#3745=CIRCLE('',#9664,0.7);
#3746=CIRCLE('',#9665,0.7);
#4347=VERTEX_POINT('',#14769);
#4348=VERTEX_POINT('',#14771);
#4349=VERTEX_POINT('',#14775);
#4350=VERTEX_POINT('',#14777);
#5227=EDGE_CURVE('',#4347,#4347,#3743,.T.);
#5228=EDGE_CURVE('',#4347,#4348,#2782,.T.);
#5229=EDGE_CURVE('',#4348,#4348,#3744,.T.);
#5230=EDGE_CURVE('',#4349,#4349,#3745,.T.);
#5231=EDGE_CURVE('',#4349,#4350,#2783,.T.);
#5232=EDGE_CURVE('',#4350,#4350,#3746,.T.);
#6833=ORIENTED_EDGE('',*,*,#5227,.F.);
#6834=ORIENTED_EDGE('',*,*,#5228,.T.);
#6835=ORIENTED_EDGE('',*,*,#5229,.T.);
#6836=ORIENTED_EDGE('',*,*,#5228,.F.);
#6837=ORIENTED_EDGE('',*,*,#5230,.F.);
#6838=ORIENTED_EDGE('',*,*,#5231,.T.);
#6839=ORIENTED_EDGE('',*,*,#5232,.T.);
#6840=ORIENTED_EDGE('',*,*,#5231,.F.);
#6841=ORIENTED_EDGE('',*,*,#5230,.T.);
#6842=ORIENTED_EDGE('',*,*,#5227,.T.);
#6843=ORIENTED_EDGE('',*,*,#5232,.F.);
#6844=ORIENTED_EDGE('',*,*,#5229,.F.);
#7777=CYLINDRICAL_SURFACE('',#9660,0.505);
#7778=CYLINDRICAL_SURFACE('',#9663,0.7);
#8133=ADVANCED_FACE('',(#1530),#7777,.F.);
#8134=ADVANCED_FACE('',(#1531),#7778,.T.);
#8135=ADVANCED_FACE('',(#1532,#905),#1129,.T.);
#8136=ADVANCED_FACE('',(#1533,#906),#1130,.F.);
#8392=CLOSED_SHELL('',(#8133,#8134,#8135,#8136));
#9659=AXIS2_PLACEMENT_3D('',#14767,#11727,#11728);
#9660=AXIS2_PLACEMENT_3D('',#14768,#11729,#11730);
#9661=AXIS2_PLACEMENT_3D('',#14770,#11731,#11732);
#9662=AXIS2_PLACEMENT_3D('',#14773,#11734,#11735);
#9663=AXIS2_PLACEMENT_3D('',#14774,#11736,#11737);
#9664=AXIS2_PLACEMENT_3D('',#14776,#11738,#11739);
#9665=AXIS2_PLACEMENT_3D('',#14779,#11741,#11742);
#9666=AXIS2_PLACEMENT_3D('',#14780,#11743,#11744);
#9667=AXIS2_PLACEMENT_3D('',#14781,#11745,#11746);
#11727=DIRECTION('axis',(0.,0.,1.));
#11728=DIRECTION('refdir',(1.,0.,0.));
#11729=DIRECTION('center_axis',(0.,1.,0.));
#11730=DIRECTION('ref_axis',(1.,0.,0.));
#11731=DIRECTION('center_axis',(0.,-1.,0.));
#11732=DIRECTION('ref_axis',(1.,0.,0.));
#11733=DIRECTION('',(0.,-1.,0.));
#11734=DIRECTION('center_axis',(0.,-1.,0.));
#11735=DIRECTION('ref_axis',(1.,0.,0.));
#11736=DIRECTION('center_axis',(0.,1.,0.));
#11737=DIRECTION('ref_axis',(1.,0.,0.));
#11738=DIRECTION('center_axis',(0.,1.,0.));
#11739=DIRECTION('ref_axis',(1.,0.,0.));
#11740=DIRECTION('',(0.,-1.,0.));
#11741=DIRECTION('center_axis',(0.,1.,0.));
#11742=DIRECTION('ref_axis',(1.,0.,0.));
#11743=DIRECTION('center_axis',(0.,1.,0.));
#11744=DIRECTION('ref_axis',(1.,0.,0.));
#11745=DIRECTION('center_axis',(0.,1.,0.));
#11746=DIRECTION('ref_axis',(1.,0.,0.));
#14767=CARTESIAN_POINT('',(0.,0.,0.));
#14768=CARTESIAN_POINT('Origin',(0.,14.1,3.5));
#14769=CARTESIAN_POINT('',(-0.505,14.55,3.5));
#14770=CARTESIAN_POINT('Origin',(0.,14.55,3.5));
#14771=CARTESIAN_POINT('',(-0.505,14.1,3.5));
#14772=CARTESIAN_POINT('',(-0.505,14.1,3.5));
#14773=CARTESIAN_POINT('Origin',(0.,14.1,3.5));
#14774=CARTESIAN_POINT('Origin',(0.,14.1,3.5));
#14775=CARTESIAN_POINT('',(-0.7,14.55,3.5));
#14776=CARTESIAN_POINT('Origin',(0.,14.55,3.5));
#14777=CARTESIAN_POINT('',(-0.7,14.1,3.5));
#14778=CARTESIAN_POINT('',(-0.7,14.1,3.5));
#14779=CARTESIAN_POINT('Origin',(0.,14.1,3.5));
#14780=CARTESIAN_POINT('Origin',(0.,14.55,3.5));
#14781=CARTESIAN_POINT('Origin',(0.,14.1,3.5));
#16173=UNCERTAINTY_MEASURE_WITH_UNIT(LENGTH_MEASURE(0.001),#16282,
'DISTANCE_ACCURACY_VALUE',
'Maximum model space distance between geometric entities at asserted c
onnectivities');
#16212=UNCERTAINTY_MEASURE_WITH_UNIT(LENGTH_MEASURE(0.001),#16282,
'DISTANCE_ACCURACY_VALUE',
'Maximum model space distance between geometric entities at asserted c
onnectivities');
#16242=(
GEOMETRIC_REPRESENTATION_CONTEXT(3)
GLOBAL_UNCERTAINTY_ASSIGNED_CONTEXT((#16173))
GLOBAL_UNIT_ASSIGNED_CONTEXT((#16282,#16284,#16285))
REPRESENTATION_CONTEXT('','3D')
);
#16281=(
GEOMETRIC_REPRESENTATION_CONTEXT(3)
GLOBAL_UNCERTAINTY_ASSIGNED_CONTEXT((#16212))
GLOBAL_UNIT_ASSIGNED_CONTEXT((#16282,#16284,#16285))
REPRESENTATION_CONTEXT('','3D')
);
#16282=(
LENGTH_UNIT()
NAMED_UNIT(*)
SI_UNIT(.CENTI.,.METRE.)
);
#16284=(
NAMED_UNIT(*)
PLANE_ANGLE_UNIT()
SI_UNIT($,.RADIAN.)
);
#16285=(
NAMED_UNIT(*)
SI_UNIT($,.STERADIAN.)
SOLID_ANGLE_UNIT()
);
#16315=SHAPE_DEFINITION_REPRESENTATION(#16409,#16548);
#16409=PRODUCT_DEFINITION_SHAPE('',$,#16617);
#16548=SHAPE_REPRESENTATION('',(#9659),#16242);
#16587=PRODUCT_DEFINITION_CONTEXT('part definition',#16793,'design');
#16617=PRODUCT_DEFINITION('Inner race spacer (2)','Inner race spacer (2)',
#16685,#16587);
#16685=PRODUCT_DEFINITION_FORMATION('',$,#16824);
#16793=APPLICATION_CONTEXT(
'Core Data for Automotive Mechanical Design Process');
#16794=PRODUCT_CONTEXT('part definition',#16793,'mechanical');
#16824=PRODUCT('Inner race spacer (2)','Inner race spacer (2)',
'Inner race spacer (2)',(#16794));
#16926=COLOUR_RGB('Grey',0.48,0.52,0.57);
#16927=FILL_AREA_STYLE_COLOUR('',#16926);
#16928=FILL_AREA_STYLE('',(#16927));
#16929=SURFACE_STYLE_FILL_AREA(#16928);
#16930=SURFACE_SIDE_STYLE('',(#16929));
#16931=SURFACE_STYLE_USAGE(.BOTH.,#16930);
#16932=PRESENTATION_STYLE_ASSIGNMENT((#16931));
ENDSEC;
END-ISO-10303-21;
